ISO-10303-21;
HEADER;
/* Generated by software containing ST-Developer
 * from STEP Tools, Inc. (www.steptools.com) 
 */

FILE_DESCRIPTION(
/* description */ (''),
/* implementation_level */ '2;1');

FILE_NAME(
/* name */ 'Motor.step',
/* time_stamp */ '2026-10-19T02:00:06+06:00',
/* author */ (''),
/* organization */ (''),
/* preprocessor_version */ 'ST-DEVELOPER v20.2',
/* originating_system */ 'Autodesk Translation Framework v15.15.0.0',
/* authorisation */ '');

FILE_SCHEMA (('AUTOMOTIVE_DESIGN { 1 0 10303 214 3 1 1 }'));
ENDSEC;

DATA;
#10=MECHANICAL_DESIGN_GEOMETRIC_PRESENTATION_REPRESENTATION('',(#113),#4833);
#91=SHAPE_REPRESENTATION_RELATIONSHIP('SRR','None',#4882,#102);
#102=ADVANCED_BREP_SHAPE_REPRESENTATION('',(#124),#4830);
#113=STYLED_ITEM('',(#5006),#124);
#124=MANIFOLD_SOLID_BREP('Motor',#2695);
#160=FACE_BOUND('',#607,.T.);
#244=PLANE('',#3044);
#245=PLANE('',#3045);
#246=PLANE('',#3046);
#247=PLANE('',#3047);
#248=PLANE('',#3048);
#249=PLANE('',#3049);
#250=PLANE('',#3050);
#251=PLANE('',#3051);
#252=PLANE('',#3052);
#253=PLANE('',#3053);
#254=PLANE('',#3054);
#401=FACE_OUTER_BOUND('',#595,.T.);
#402=FACE_OUTER_BOUND('',#596,.T.);
#403=FACE_OUTER_BOUND('',#597,.T.);
#404=FACE_OUTER_BOUND('',#598,.T.);
#405=FACE_OUTER_BOUND('',#599,.T.);
#406=FACE_OUTER_BOUND('',#600,.T.);
#407=FACE_OUTER_BOUND('',#601,.T.);
#408=FACE_OUTER_BOUND('',#602,.T.);
#409=FACE_OUTER_BOUND('',#603,.T.);
#410=FACE_OUTER_BOUND('',#604,.T.);
#411=FACE_OUTER_BOUND('',#605,.T.);
#412=FACE_OUTER_BOUND('',#606,.T.);
#595=EDGE_LOOP('',(#2353,#2354,#2355,#2356));
#596=EDGE_LOOP('',(#2357));
#597=EDGE_LOOP('',(#2358,#2359,#2360,#2361));
#598=EDGE_LOOP('',(#2362,#2363,#2364,#2365,#2366,#2367,#2368,#2369));
#599=EDGE_LOOP('',(#2370,#2371,#2372,#2373));
#600=EDGE_LOOP('',(#2374,#2375,#2376,#2377));
#601=EDGE_LOOP('',(#2378,#2379,#2380,#2381));
#602=EDGE_LOOP('',(#2382,#2383,#2384,#2385));
#603=EDGE_LOOP('',(#2386,#2387,#2388,#2389));
#604=EDGE_LOOP('',(#2390,#2391,#2392,#2393));
#605=EDGE_LOOP('',(#2394,#2395,#2396,#2397));
#606=EDGE_LOOP('',(#2398,#2399,#2400,#2401,#2402,#2403,#2404,#2405));
#607=EDGE_LOOP('',(#2406));
#829=LINE('',#4671,#1083);
#830=LINE('',#4677,#1084);
#831=LINE('',#4679,#1085);
#832=LINE('',#4681,#1086);
#833=LINE('',#4682,#1087);
#834=LINE('',#4685,#1088);
#835=LINE('',#4687,#1089);
#836=LINE('',#4689,#1090);
#837=LINE('',#4691,#1091);
#838=LINE('',#4693,#1092);
#839=LINE('',#4695,#1093);
#840=LINE('',#4696,#1094);
#841=LINE('',#4699,#1095);
#842=LINE('',#4700,#1096);
#843=LINE('',#4703,#1097);
#844=LINE('',#4704,#1098);
#845=LINE('',#4708,#1099);
#846=LINE('',#4709,#1100);
#847=LINE('',#4710,#1101);
#848=LINE('',#4713,#1102);
#849=LINE('',#4714,#1103);
#850=LINE('',#4717,#1104);
#851=LINE('',#4718,#1105);
#852=LINE('',#4720,#1106);
#853=LINE('',#4722,#1107);
#1083=VECTOR('',#3738,17.5);
#1084=VECTOR('',#3745,10.);
#1085=VECTOR('',#3746,10.);
#1086=VECTOR('',#3747,10.);
#1087=VECTOR('',#3748,10.);
#1088=VECTOR('',#3751,10.);
#1089=VECTOR('',#3752,10.);
#1090=VECTOR('',#3753,10.);
#1091=VECTOR('',#3754,10.);
#1092=VECTOR('',#3755,10.);
#1093=VECTOR('',#3756,10.);
#1094=VECTOR('',#3757,10.);
#1095=VECTOR('',#3760,10.);
#1096=VECTOR('',#3761,10.);
#1097=VECTOR('',#3764,10.);
#1098=VECTOR('',#3765,10.);
#1099=VECTOR('',#3768,10.);
#1100=VECTOR('',#3769,10.);
#1101=VECTOR('',#3770,10.);
#1102=VECTOR('',#3773,10.);
#1103=VECTOR('',#3774,10.);
#1104=VECTOR('',#3777,10.);
#1105=VECTOR('',#3778,10.);
#1106=VECTOR('',#3781,10.);
#1107=VECTOR('',#3784,10.);
#1197=CIRCLE('',#3042,17.5);
#1198=CIRCLE('',#3043,17.5);
#1389=VERTEX_POINT('',#4668);
#1390=VERTEX_POINT('',#4670);
#1391=VERTEX_POINT('',#4675);
#1392=VERTEX_POINT('',#4676);
#1393=VERTEX_POINT('',#4678);
#1394=VERTEX_POINT('',#4680);
#1395=VERTEX_POINT('',#4684);
#1396=VERTEX_POINT('',#4686);
#1397=VERTEX_POINT('',#4688);
#1398=VERTEX_POINT('',#4690);
#1399=VERTEX_POINT('',#4692);
#1400=VERTEX_POINT('',#4694);
#1401=VERTEX_POINT('',#4698);
#1402=VERTEX_POINT('',#4702);
#1403=VERTEX_POINT('',#4706);
#1404=VERTEX_POINT('',#4707);
#1405=VERTEX_POINT('',#4712);
#1406=VERTEX_POINT('',#4716);
#1717=EDGE_CURVE('',#1389,#1389,#1197,.T.);
#1718=EDGE_CURVE('',#1389,#1390,#829,.T.);
#1719=EDGE_CURVE('',#1390,#1390,#1198,.T.);
#1720=EDGE_CURVE('',#1391,#1392,#830,.T.);
#1721=EDGE_CURVE('',#1392,#1393,#831,.T.);
#1722=EDGE_CURVE('',#1393,#1394,#832,.T.);
#1723=EDGE_CURVE('',#1394,#1391,#833,.T.);
#1724=EDGE_CURVE('',#1393,#1395,#834,.T.);
#1725=EDGE_CURVE('',#1396,#1395,#835,.T.);
#1726=EDGE_CURVE('',#1396,#1397,#836,.T.);
#1727=EDGE_CURVE('',#1398,#1397,#837,.T.);
#1728=EDGE_CURVE('',#1398,#1399,#838,.T.);
#1729=EDGE_CURVE('',#1400,#1399,#839,.T.);
#1730=EDGE_CURVE('',#1400,#1394,#840,.T.);
#1731=EDGE_CURVE('',#1401,#1392,#841,.T.);
#1732=EDGE_CURVE('',#1395,#1401,#842,.T.);
#1733=EDGE_CURVE('',#1401,#1402,#843,.T.);
#1734=EDGE_CURVE('',#1402,#1396,#844,.T.);
#1735=EDGE_CURVE('',#1403,#1404,#845,.T.);
#1736=EDGE_CURVE('',#1404,#1400,#846,.T.);
#1737=EDGE_CURVE('',#1399,#1403,#847,.T.);
#1738=EDGE_CURVE('',#1405,#1398,#848,.T.);
#1739=EDGE_CURVE('',#1403,#1405,#849,.T.);
#1740=EDGE_CURVE('',#1406,#1405,#850,.T.);
#1741=EDGE_CURVE('',#1397,#1406,#851,.T.);
#1742=EDGE_CURVE('',#1406,#1402,#852,.T.);
#1743=EDGE_CURVE('',#1391,#1404,#853,.T.);
#2353=ORIENTED_EDGE('',*,*,#1717,.F.);
#2354=ORIENTED_EDGE('',*,*,#1718,.T.);
#2355=ORIENTED_EDGE('',*,*,#1719,.F.);
#2356=ORIENTED_EDGE('',*,*,#1718,.F.);
#2357=ORIENTED_EDGE('',*,*,#1717,.T.);
#2358=ORIENTED_EDGE('',*,*,#1720,.T.);
#2359=ORIENTED_EDGE('',*,*,#1721,.T.);
#2360=ORIENTED_EDGE('',*,*,#1722,.T.);
#2361=ORIENTED_EDGE('',*,*,#1723,.T.);
#2362=ORIENTED_EDGE('',*,*,#1722,.F.);
#2363=ORIENTED_EDGE('',*,*,#1724,.T.);
#2364=ORIENTED_EDGE('',*,*,#1725,.F.);
#2365=ORIENTED_EDGE('',*,*,#1726,.T.);
#2366=ORIENTED_EDGE('',*,*,#1727,.F.);
#2367=ORIENTED_EDGE('',*,*,#1728,.T.);
#2368=ORIENTED_EDGE('',*,*,#1729,.F.);
#2369=ORIENTED_EDGE('',*,*,#1730,.T.);
#2370=ORIENTED_EDGE('',*,*,#1721,.F.);
#2371=ORIENTED_EDGE('',*,*,#1731,.F.);
#2372=ORIENTED_EDGE('',*,*,#1732,.F.);
#2373=ORIENTED_EDGE('',*,*,#1724,.F.);
#2374=ORIENTED_EDGE('',*,*,#1733,.T.);
#2375=ORIENTED_EDGE('',*,*,#1734,.T.);
#2376=ORIENTED_EDGE('',*,*,#1725,.T.);
#2377=ORIENTED_EDGE('',*,*,#1732,.T.);
#2378=ORIENTED_EDGE('',*,*,#1735,.T.);
#2379=ORIENTED_EDGE('',*,*,#1736,.T.);
#2380=ORIENTED_EDGE('',*,*,#1729,.T.);
#2381=ORIENTED_EDGE('',*,*,#1737,.T.);
#2382=ORIENTED_EDGE('',*,*,#1737,.F.);
#2383=ORIENTED_EDGE('',*,*,#1728,.F.);
#2384=ORIENTED_EDGE('',*,*,#1738,.F.);
#2385=ORIENTED_EDGE('',*,*,#1739,.F.);
#2386=ORIENTED_EDGE('',*,*,#1740,.T.);
#2387=ORIENTED_EDGE('',*,*,#1738,.T.);
#2388=ORIENTED_EDGE('',*,*,#1727,.T.);
#2389=ORIENTED_EDGE('',*,*,#1741,.T.);
#2390=ORIENTED_EDGE('',*,*,#1734,.F.);
#2391=ORIENTED_EDGE('',*,*,#1742,.F.);
#2392=ORIENTED_EDGE('',*,*,#1741,.F.);
#2393=ORIENTED_EDGE('',*,*,#1726,.F.);
#2394=ORIENTED_EDGE('',*,*,#1723,.F.);
#2395=ORIENTED_EDGE('',*,*,#1730,.F.);
#2396=ORIENTED_EDGE('',*,*,#1736,.F.);
#2397=ORIENTED_EDGE('',*,*,#1743,.F.);
#2398=ORIENTED_EDGE('',*,*,#1720,.F.);
#2399=ORIENTED_EDGE('',*,*,#1743,.T.);
#2400=ORIENTED_EDGE('',*,*,#1735,.F.);
#2401=ORIENTED_EDGE('',*,*,#1739,.T.);
#2402=ORIENTED_EDGE('',*,*,#1740,.F.);
#2403=ORIENTED_EDGE('',*,*,#1742,.T.);
#2404=ORIENTED_EDGE('',*,*,#1733,.F.);
#2405=ORIENTED_EDGE('',*,*,#1731,.T.);
#2406=ORIENTED_EDGE('',*,*,#1719,.T.);
#2522=CYLINDRICAL_SURFACE('',#3041,17.5);
#2659=ADVANCED_FACE('',(#401),#2522,.T.);
#2660=ADVANCED_FACE('',(#402),#244,.T.);
#2661=ADVANCED_FACE('',(#403),#245,.T.);
#2662=ADVANCED_FACE('',(#404),#246,.F.);
#2663=ADVANCED_FACE('',(#405),#247,.T.);
#2664=ADVANCED_FACE('',(#406),#248,.T.);
#2665=ADVANCED_FACE('',(#407),#249,.T.);
#2666=ADVANCED_FACE('',(#408),#250,.T.);
#2667=ADVANCED_FACE('',(#409),#251,.T.);
#2668=ADVANCED_FACE('',(#410),#252,.T.);
#2669=ADVANCED_FACE('',(#411),#253,.T.);
#2670=ADVANCED_FACE('',(#412,#160),#254,.T.);
#2695=CLOSED_SHELL('',(#2659,#2660,#2661,#2662,#2663,#2664,#2665,#2666,
#2667,#2668,#2669,#2670));
#3040=AXIS2_PLACEMENT_3D('',#4666,#3732,#3733);
#3041=AXIS2_PLACEMENT_3D('',#4667,#3734,#3735);
#3042=AXIS2_PLACEMENT_3D('',#4669,#3736,#3737);
#3043=AXIS2_PLACEMENT_3D('',#4672,#3739,#3740);
#3044=AXIS2_PLACEMENT_3D('',#4673,#3741,#3742);
#3045=AXIS2_PLACEMENT_3D('',#4674,#3743,#3744);
#3046=AXIS2_PLACEMENT_3D('',#4683,#3749,#3750);
#3047=AXIS2_PLACEMENT_3D('',#4697,#3758,#3759);
#3048=AXIS2_PLACEMENT_3D('',#4701,#3762,#3763);
#3049=AXIS2_PLACEMENT_3D('',#4705,#3766,#3767);
#3050=AXIS2_PLACEMENT_3D('',#4711,#3771,#3772);
#3051=AXIS2_PLACEMENT_3D('',#4715,#3775,#3776);
#3052=AXIS2_PLACEMENT_3D('',#4719,#3779,#3780);
#3053=AXIS2_PLACEMENT_3D('',#4721,#3782,#3783);
#3054=AXIS2_PLACEMENT_3D('',#4723,#3785,#3786);
#3732=DIRECTION('axis',(0.,0.,1.));
#3733=DIRECTION('refdir',(1.,0.,0.));
#3734=DIRECTION('center_axis',(1.,0.,0.));
#3735=DIRECTION('ref_axis',(0.,1.,0.));
#3736=DIRECTION('center_axis',(1.,0.,0.));
#3737=DIRECTION('ref_axis',(0.,1.,0.));
#3738=DIRECTION('',(-1.,0.,0.));
#3739=DIRECTION('center_axis',(-1.,0.,0.));
#3740=DIRECTION('ref_axis',(0.,1.,0.));
#3741=DIRECTION('center_axis',(1.,0.,0.));
#3742=DIRECTION('ref_axis',(0.,1.,0.));
#3743=DIRECTION('center_axis',(0.,0.707106781186548,-0.707106781186548));
#3744=DIRECTION('ref_axis',(-1.,0.,0.));
#3745=DIRECTION('',(0.,-0.707106781186548,-0.707106781186548));
#3746=DIRECTION('',(-1.,0.,0.));
#3747=DIRECTION('',(0.,0.707106781186548,0.707106781186548));
#3748=DIRECTION('',(1.,0.,0.));
#3749=DIRECTION('center_axis',(1.,0.,0.));
#3750=DIRECTION('ref_axis',(0.,1.,0.));
#3751=DIRECTION('',(0.,-1.,3.70074341541719E-17));
#3752=DIRECTION('',(0.,0.707106781186548,-0.707106781186548));
#3753=DIRECTION('',(0.,0.,1.));
#3754=DIRECTION('',(0.,-0.707106781186548,-0.707106781186548));
#3755=DIRECTION('',(0.,1.,0.));
#3756=DIRECTION('',(0.,-0.707106781186548,0.707106781186548));
#3757=DIRECTION('',(0.,0.,-1.));
#3758=DIRECTION('center_axis',(0.,-3.70074341541719E-17,-1.));
#3759=DIRECTION('ref_axis',(0.,1.,-3.70074341541719E-17));
#3760=DIRECTION('',(0.,1.,-3.70074341541719E-17));
#3761=DIRECTION('',(1.,0.,0.));
#3762=DIRECTION('center_axis',(0.,-0.707106781186548,-0.707106781186548));
#3763=DIRECTION('ref_axis',(-1.,0.,0.));
#3764=DIRECTION('',(0.,-0.707106781186548,0.707106781186548));
#3765=DIRECTION('',(-1.,0.,0.));
#3766=DIRECTION('center_axis',(0.,0.707106781186548,0.707106781186548));
#3767=DIRECTION('ref_axis',(1.,0.,0.));
#3768=DIRECTION('',(0.,0.707106781186548,-0.707106781186548));
#3769=DIRECTION('',(-1.,0.,0.));
#3770=DIRECTION('',(1.,0.,0.));
#3771=DIRECTION('center_axis',(0.,0.,1.));
#3772=DIRECTION('ref_axis',(0.,-1.,0.));
#3773=DIRECTION('',(-1.,0.,0.));
#3774=DIRECTION('',(0.,-1.,0.));
#3775=DIRECTION('center_axis',(0.,-0.707106781186548,0.707106781186548));
#3776=DIRECTION('ref_axis',(1.,0.,0.));
#3777=DIRECTION('',(0.,0.707106781186548,0.707106781186548));
#3778=DIRECTION('',(1.,0.,0.));
#3779=DIRECTION('center_axis',(0.,-1.,0.));
#3780=DIRECTION('ref_axis',(0.,0.,-1.));
#3781=DIRECTION('',(0.,0.,-1.));
#3782=DIRECTION('center_axis',(0.,1.,0.));
#3783=DIRECTION('ref_axis',(0.,0.,1.));
#3784=DIRECTION('',(0.,0.,1.));
#3785=DIRECTION('center_axis',(1.,0.,0.));
#3786=DIRECTION('ref_axis',(0.,0.,-1.));
#4666=CARTESIAN_POINT('',(0.,0.,0.));
#4667=CARTESIAN_POINT('Origin',(20.,59.9999999999895,2.1138646388863E-12));
#4668=CARTESIAN_POINT('',(85.,42.4999999999895,2.11172150698779E-12));
#4669=CARTESIAN_POINT('Origin',(85.,59.9999999999895,2.1138646388863E-12));
#4670=CARTESIAN_POINT('',(20.,42.4999999999895,2.11172150698779E-12));
#4671=CARTESIAN_POINT('',(20.,42.4999999999895,2.11172150698779E-12));
#4672=CARTESIAN_POINT('Origin',(20.,59.9999999999895,2.1138646388863E-12));
#4673=CARTESIAN_POINT('Origin',(85.,59.9999999999895,2.1138646388863E-12));
#4674=CARTESIAN_POINT('Origin',(-90.,84.9999999999895,-14.9999999999979));
#4675=CARTESIAN_POINT('',(20.,89.9999999999895,-9.99999999999789));
#4676=CARTESIAN_POINT('',(20.,79.9999999999895,-19.9999999999979));
#4677=CARTESIAN_POINT('',(20.,82.4999999999895,-17.4999999999979));
#4678=CARTESIAN_POINT('',(-90.,79.9999999999895,-19.9999999999979));
#4679=CARTESIAN_POINT('',(-90.,79.9999999999895,-19.9999999999979));
#4680=CARTESIAN_POINT('',(-90.,89.9999999999895,-9.99999999999789));
#4681=CARTESIAN_POINT('',(-90.,82.4999999999895,-17.4999999999979));
#4682=CARTESIAN_POINT('',(-90.,89.9999999999895,-9.99999999999789));
#4683=CARTESIAN_POINT('Origin',(-90.,59.9999999999895,2.11275441586167E-12));
#4684=CARTESIAN_POINT('',(-90.,39.9999999999895,-19.9999999999979));
#4685=CARTESIAN_POINT('',(-90.,89.9999999999895,-19.9999999999979));
#4686=CARTESIAN_POINT('',(-90.,29.9999999999895,-9.99999999999789));
#4687=CARTESIAN_POINT('',(-90.,37.4999999999895,-17.4999999999979));
#4688=CARTESIAN_POINT('',(-90.,29.9999999999895,10.0000000000021));
#4689=CARTESIAN_POINT('',(-90.,29.9999999999895,-19.9999999999979));
#4690=CARTESIAN_POINT('',(-90.,39.9999999999895,20.0000000000021));
#4691=CARTESIAN_POINT('',(-90.,37.4999999999895,17.5000000000021));
#4692=CARTESIAN_POINT('',(-90.,79.9999999999895,20.0000000000021));
#4693=CARTESIAN_POINT('',(-90.,29.9999999999895,20.0000000000021));
#4694=CARTESIAN_POINT('',(-90.,89.9999999999895,10.0000000000021));
#4695=CARTESIAN_POINT('',(-90.,82.4999999999895,17.5000000000021));
#4696=CARTESIAN_POINT('',(-90.,89.9999999999895,20.0000000000021));
#4697=CARTESIAN_POINT('Origin',(-90.,29.9999999999895,-19.9999999999979));
#4698=CARTESIAN_POINT('',(20.,39.9999999999895,-19.9999999999979));
#4699=CARTESIAN_POINT('',(20.,89.9999999999895,-19.9999999999979));
#4700=CARTESIAN_POINT('',(-90.,39.9999999999895,-19.9999999999979));
#4701=CARTESIAN_POINT('Origin',(-90.,34.9999999999895,-14.9999999999979));
#4702=CARTESIAN_POINT('',(20.,29.9999999999895,-9.99999999999789));
#4703=CARTESIAN_POINT('',(20.,37.4999999999895,-17.4999999999979));
#4704=CARTESIAN_POINT('',(-90.,29.9999999999895,-9.99999999999789));
#4705=CARTESIAN_POINT('Origin',(-90.,84.9999999999895,15.0000000000021));
#4706=CARTESIAN_POINT('',(20.,79.9999999999895,20.0000000000021));
#4707=CARTESIAN_POINT('',(20.,89.9999999999895,10.0000000000021));
#4708=CARTESIAN_POINT('',(20.,82.4999999999895,17.5000000000021));
#4709=CARTESIAN_POINT('',(-90.,89.9999999999895,10.0000000000021));
#4710=CARTESIAN_POINT('',(-90.,79.9999999999895,20.0000000000021));
#4711=CARTESIAN_POINT('Origin',(-90.,89.9999999999895,20.0000000000021));
#4712=CARTESIAN_POINT('',(20.,39.9999999999895,20.0000000000021));
#4713=CARTESIAN_POINT('',(-90.,39.9999999999895,20.0000000000021));
#4714=CARTESIAN_POINT('',(20.,29.9999999999895,20.0000000000021));
#4715=CARTESIAN_POINT('Origin',(-90.,34.9999999999895,15.0000000000021));
#4716=CARTESIAN_POINT('',(20.,29.9999999999895,10.0000000000021));
#4717=CARTESIAN_POINT('',(20.,37.4999999999895,17.5000000000021));
#4718=CARTESIAN_POINT('',(-90.,29.9999999999895,10.0000000000021));
#4719=CARTESIAN_POINT('Origin',(-90.,29.9999999999895,20.0000000000021));
#4720=CARTESIAN_POINT('',(20.,29.9999999999895,-19.9999999999979));
#4721=CARTESIAN_POINT('Origin',(-90.,89.9999999999895,-19.9999999999979));
#4722=CARTESIAN_POINT('',(20.,89.9999999999895,20.0000000000021));
#4723=CARTESIAN_POINT('Origin',(20.,59.9999999999895,2.11164419283705E-12));
#4817=UNCERTAINTY_MEASURE_WITH_UNIT(LENGTH_MEASURE(0.01),#4834,
'DISTANCE_ACCURACY_VALUE',
'Maximum model space distance between geometric entities at asserted c
onnectivities');
#4820=UNCERTAINTY_MEASURE_WITH_UNIT(LENGTH_MEASURE(0.01),#4834,
'DISTANCE_ACCURACY_VALUE',
'Maximum model space distance between geometric entities at asserted c
onnectivities');
#4830=(
GEOMETRIC_REPRESENTATION_CONTEXT(3)
GLOBAL_UNCERTAINTY_ASSIGNED_CONTEXT((#4817))
GLOBAL_UNIT_ASSIGNED_CONTEXT((#4834,#4836,#4837))
REPRESENTATION_CONTEXT('','3D')
);
#4833=(
GEOMETRIC_REPRESENTATION_CONTEXT(3)
GLOBAL_UNCERTAINTY_ASSIGNED_CONTEXT((#4820))
GLOBAL_UNIT_ASSIGNED_CONTEXT((#4834,#4836,#4837))
REPRESENTATION_CONTEXT('','3D')
);
#4834=(
LENGTH_UNIT()
NAMED_UNIT(*)
SI_UNIT(.MILLI.,.METRE.)
);
#4836=(
NAMED_UNIT(*)
PLANE_ANGLE_UNIT()
SI_UNIT($,.RADIAN.)
);
#4837=(
NAMED_UNIT(*)
SI_UNIT($,.STERADIAN.)
SOLID_ANGLE_UNIT()
);
#4847=SHAPE_DEFINITION_REPRESENTATION(#4859,#4882);
#4859=PRODUCT_DEFINITION_SHAPE('',$,#4895);
#4882=SHAPE_REPRESENTATION('',(#3040),#4830);
#4885=PRODUCT_DEFINITION_CONTEXT('part definition',#4923,'design');
#4895=PRODUCT_DEFINITION('Motor','Motor',#4907,#4885);
#4907=PRODUCT_DEFINITION_FORMATION('',$,#4934);
#4923=APPLICATION_CONTEXT(
'Core Data for Automotive Mechanical Design Process');
#4924=PRODUCT_CONTEXT('part definition',#4923,'mechanical');
#4934=PRODUCT('Motor','Motor',$,(#4924));
#5000=COLOUR_RGB('Off White',0.89,0.88,0.83);
#5001=FILL_AREA_STYLE_COLOUR('',#5000);
#5002=FILL_AREA_STYLE('',(#5001));
#5003=SURFACE_STYLE_FILL_AREA(#5002);
#5004=SURFACE_SIDE_STYLE('',(#5003));
#5005=SURFACE_STYLE_USAGE(.BOTH.,#5004);
#5006=PRESENTATION_STYLE_ASSIGNMENT((#5005));
ENDSEC;
END-ISO-10303-21;
